ISO-10303-21;
HEADER;
/* Generated by software containing ST-Developer
 * from STEP Tools, Inc. (www.steptools.com) 
 */

FILE_DESCRIPTION(
/* description */ ('PAT-091'),
/* implementation_level */ '2;1');

FILE_NAME(
/* name */ 'Guide shaft (3).step',
/* time_stamp */ '2026-10-27T15:34:44-07:00',
/* author */ (''),
/* organization */ (''),
/* preprocessor_version */ 'ST-DEVELOPER v20.2',
/* originating_system */ 'Autodesk Translation Framework v15.17.0.0',
/* authorisation */ '');

FILE_SCHEMA (('AUTOMOTIVE_DESIGN { 1 0 10303 214 3 1 1 }'));
ENDSEC;

DATA;
#10=MECHANICAL_DESIGN_GEOMETRIC_PRESENTATION_REPRESENTATION('',(#993),#25100);
#773=SHAPE_REPRESENTATION_RELATIONSHIP('SRR','None',#25535,#883);
#883=ADVANCED_BREP_SHAPE_REPRESENTATION('',(#1116),#25005);
#993=STYLED_ITEM('',(#26191),#1116);
#1116=MANIFOLD_SOLID_BREP('Body1',#13271);
#1748=PLANE('',#15022);
#1749=PLANE('',#15023);
#2272=FACE_OUTER_BOUND('',#3252,.T.);
#2273=FACE_OUTER_BOUND('',#3253,.T.);
#2274=FACE_OUTER_BOUND('',#3254,.T.);
#3252=EDGE_LOOP('',(#9896,#9897,#9898,#9899));
#3253=EDGE_LOOP('',(#9900));
#3254=EDGE_LOOP('',(#9901));
#4387=LINE('',#21982,#5127);
#5127=VECTOR('',#17603,0.6);
#5803=CIRCLE('',#15020,0.6);
#5804=CIRCLE('',#15021,0.6);
#6690=VERTEX_POINT('',#21979);
#6691=VERTEX_POINT('',#21981);
#7883=EDGE_CURVE('',#6690,#6690,#5803,.T.);
#7884=EDGE_CURVE('',#6690,#6691,#4387,.T.);
#7885=EDGE_CURVE('',#6691,#6691,#5804,.T.);
#9896=ORIENTED_EDGE('',*,*,#7883,.F.);
#9897=ORIENTED_EDGE('',*,*,#7884,.T.);
#9898=ORIENTED_EDGE('',*,*,#7885,.T.);
#9899=ORIENTED_EDGE('',*,*,#7884,.F.);
#9900=ORIENTED_EDGE('',*,*,#7883,.T.);
#9901=ORIENTED_EDGE('',*,*,#7885,.F.);
#12172=CYLINDRICAL_SURFACE('',#15019,0.6);
#12639=ADVANCED_FACE('',(#2272),#12172,.T.);
#12640=ADVANCED_FACE('',(#2273),#1748,.T.);
#12641=ADVANCED_FACE('',(#2274),#1749,.F.);
#13271=CLOSED_SHELL('',(#12639,#12640,#12641));
#15018=AXIS2_PLACEMENT_3D('',#21977,#17597,#17598);
#15019=AXIS2_PLACEMENT_3D('',#21978,#17599,#17600);
#15020=AXIS2_PLACEMENT_3D('',#21980,#17601,#17602);
#15021=AXIS2_PLACEMENT_3D('',#21983,#17604,#17605);
#15022=AXIS2_PLACEMENT_3D('',#21984,#17606,#17607);
#15023=AXIS2_PLACEMENT_3D('',#21985,#17608,#17609);
#17597=DIRECTION('axis',(0.,0.,1.));
#17598=DIRECTION('refdir',(1.,0.,0.));
#17599=DIRECTION('center_axis',(1.,0.,0.));
#17600=DIRECTION('ref_axis',(0.,0.,-1.));
#17601=DIRECTION('center_axis',(1.,0.,0.));
#17602=DIRECTION('ref_axis',(0.,0.,-1.));
#17603=DIRECTION('',(-1.,0.,0.));
#17604=DIRECTION('center_axis',(1.,0.,0.));
#17605=DIRECTION('ref_axis',(0.,0.,-1.));
#17606=DIRECTION('center_axis',(1.,0.,0.));
#17607=DIRECTION('ref_axis',(0.,0.,-1.));
#17608=DIRECTION('center_axis',(1.,0.,0.));
#17609=DIRECTION('ref_axis',(0.,0.,-1.));
#21977=CARTESIAN_POINT('',(0.,0.,0.));
#21978=CARTESIAN_POINT('Origin',(-1.,3.,16.));
#21979=CARTESIAN_POINT('',(47.,3.,16.6));
#21980=CARTESIAN_POINT('Origin',(47.,3.,16.));
#21981=CARTESIAN_POINT('',(-1.,3.,16.6));
#21982=CARTESIAN_POINT('',(-1.,3.,16.6));
#21983=CARTESIAN_POINT('Origin',(-1.,3.,16.));
#21984=CARTESIAN_POINT('Origin',(47.,3.,16.));
#21985=CARTESIAN_POINT('Origin',(-1.,3.,16.));
#24884=UNCERTAINTY_MEASURE_WITH_UNIT(LENGTH_MEASURE(0.001),#25101,
'DISTANCE_ACCURACY_VALUE',
'Maximum model space distance between geometric entities at asserted c
onnectivities');
#24979=UNCERTAINTY_MEASURE_WITH_UNIT(LENGTH_MEASURE(0.001),#25101,
'DISTANCE_ACCURACY_VALUE',
'Maximum model space distance between geometric entities at asserted c
onnectivities');
#25005=(
GEOMETRIC_REPRESENTATION_CONTEXT(3)
GLOBAL_UNCERTAINTY_ASSIGNED_CONTEXT((#24884))
GLOBAL_UNIT_ASSIGNED_CONTEXT((#25101,#25103,#25104))
REPRESENTATION_CONTEXT('','3D')
);
#25100=(
GEOMETRIC_REPRESENTATION_CONTEXT(3)
GLOBAL_UNCERTAINTY_ASSIGNED_CONTEXT((#24979))
GLOBAL_UNIT_ASSIGNED_CONTEXT((#25101,#25103,#25104))
REPRESENTATION_CONTEXT('','3D')
);
#25101=(
LENGTH_UNIT()
NAMED_UNIT(*)
SI_UNIT(.CENTI.,.METRE.)
);
#25103=(
NAMED_UNIT(*)
PLANE_ANGLE_UNIT()
SI_UNIT($,.RADIAN.)
);
#25104=(
NAMED_UNIT(*)
SI_UNIT($,.STERADIAN.)
SOLID_ANGLE_UNIT()
);
#25130=SHAPE_DEFINITION_REPRESENTATION(#25250,#25535);
#25250=PRODUCT_DEFINITION_SHAPE('',$,#25656);
#25535=SHAPE_REPRESENTATION('',(#15018),#25005);
#25630=PRODUCT_DEFINITION_CONTEXT('part definition',#25992,'design');
#25656=PRODUCT_DEFINITION('Guide shaft (3)','Guide shaft (3)',#25776,#25630);
#25776=PRODUCT_DEFINITION_FORMATION('',$,#26019);
#25992=APPLICATION_CONTEXT(
'Core Data for Automotive Mechanical Design Process');
#25993=PRODUCT_CONTEXT('part definition',#25992,'mechanical');
#26019=PRODUCT('Guide shaft (3)','Guide shaft (3)','Guide shaft (3)',(#25993));
#26185=COLOUR_RGB('Grey',0.48,0.52,0.57);
#26186=FILL_AREA_STYLE_COLOUR('',#26185);
#26187=FILL_AREA_STYLE('',(#26186));
#26188=SURFACE_STYLE_FILL_AREA(#26187);
#26189=SURFACE_SIDE_STYLE('',(#26188));
#26190=SURFACE_STYLE_USAGE(.BOTH.,#26189);
#26191=PRESENTATION_STYLE_ASSIGNMENT((#26190));
ENDSEC;
END-ISO-10303-21;
